ISO-10303-21;
HEADER;
/* Generated by software containing ST-Developer
 * from STEP Tools, Inc. (www.steptools.com) 
 */

FILE_DESCRIPTION(
/* description */ ('PAT-083'),
/* implementation_level */ '2;1');

FILE_NAME(
/* name */ 'Cap Screw - M4x16.step',
/* time_stamp */ '2026-10-29T20:18:00-07:00',
/* author */ (''),
/* organization */ (''),
/* preprocessor_version */ 'ST-DEVELOPER v20.2',
/* originating_system */ 'Autodesk Translation Framework v15.17.0.0',
/* authorisation */ '');

FILE_SCHEMA (('AUTOMOTIVE_DESIGN { 1 0 10303 214 3 1 1 }'));
ENDSEC;

DATA;
#10=MECHANICAL_DESIGN_GEOMETRIC_PRESENTATION_REPRESENTATION('',(#247),#8428);
#147=ORIENTED_CLOSED_SHELL('',*,#3694,.F.);
#149=CONICAL_SURFACE('',#4290,0.325,0.785398163397448);
#150=CONICAL_SURFACE('',#4294,0.335,0.785398163397448);
#151=CONICAL_SURFACE('',#4298,0.21,0.463647609000806);
#152=CONICAL_SURFACE('',#4302,0.18,0.785398163397448);
#163=BREP_WITH_VOIDS('Body1',#3693,(#147));
#199=SHAPE_REPRESENTATION_RELATIONSHIP('SRR','None',#8533,#223);
#223=ADVANCED_BREP_SHAPE_REPRESENTATION('',(#163),#8422);
#247=STYLED_ITEM('',(#8712),#163);
#345=FACE_BOUND('',#960,.T.);
#444=PLANE('',#4288);
#445=PLANE('',#4296);
#446=PLANE('',#4304);
#447=PLANE('',#4305);
#448=PLANE('',#4306);
#449=PLANE('',#4307);
#450=PLANE('',#4308);
#451=PLANE('',#4309);
#452=PLANE('',#4310);
#453=PLANE('',#4311);
#454=PLANE('',#4312);
#652=FACE_OUTER_BOUND('',#955,.T.);
#653=FACE_OUTER_BOUND('',#956,.T.);
#654=FACE_OUTER_BOUND('',#957,.T.);
#655=FACE_OUTER_BOUND('',#958,.T.);
#656=FACE_OUTER_BOUND('',#959,.T.);
#657=FACE_OUTER_BOUND('',#961,.T.);
#658=FACE_OUTER_BOUND('',#962,.T.);
#659=FACE_OUTER_BOUND('',#963,.T.);
#660=FACE_OUTER_BOUND('',#964,.T.);
#661=FACE_OUTER_BOUND('',#965,.T.);
#662=FACE_OUTER_BOUND('',#966,.T.);
#663=FACE_OUTER_BOUND('',#967,.T.);
#664=FACE_OUTER_BOUND('',#968,.T.);
#665=FACE_OUTER_BOUND('',#969,.T.);
#666=FACE_OUTER_BOUND('',#970,.T.);
#667=FACE_OUTER_BOUND('',#971,.T.);
#668=FACE_OUTER_BOUND('',#972,.T.);
#955=EDGE_LOOP('',(#3062));
#956=EDGE_LOOP('',(#3063,#3064,#3065,#3066));
#957=EDGE_LOOP('',(#3067,#3068,#3069,#3070));
#958=EDGE_LOOP('',(#3071,#3072,#3073,#3074));
#959=EDGE_LOOP('',(#3075));
#960=EDGE_LOOP('',(#3076));
#961=EDGE_LOOP('',(#3077,#3078,#3079,#3080));
#962=EDGE_LOOP('',(#3081,#3082,#3083,#3084));
#963=EDGE_LOOP('',(#3085,#3086,#3087,#3088));
#964=EDGE_LOOP('',(#3089));
#965=EDGE_LOOP('',(#3090,#3091,#3092,#3093));
#966=EDGE_LOOP('',(#3094,#3095,#3096,#3097));
#967=EDGE_LOOP('',(#3098,#3099,#3100,#3101));
#968=EDGE_LOOP('',(#3102,#3103,#3104,#3105));
#969=EDGE_LOOP('',(#3106,#3107,#3108,#3109));
#970=EDGE_LOOP('',(#3110,#3111,#3112,#3113));
#971=EDGE_LOOP('',(#3114,#3115,#3116,#3117,#3118,#3119));
#972=EDGE_LOOP('',(#3120,#3121,#3122,#3123,#3124,#3125));
#1183=LINE('',#8000,#1427);
#1184=LINE('',#8004,#1428);
#1185=LINE('',#8008,#1429);
#1186=LINE('',#8015,#1430);
#1187=LINE('',#8019,#1431);
#1188=LINE('',#8023,#1432);
#1189=LINE('',#8028,#1433);
#1190=LINE('',#8030,#1434);
#1191=LINE('',#8032,#1435);
#1192=LINE('',#8033,#1436);
#1193=LINE('',#8036,#1437);
#1194=LINE('',#8038,#1438);
#1195=LINE('',#8039,#1439);
#1196=LINE('',#8042,#1440);
#1197=LINE('',#8044,#1441);
#1198=LINE('',#8045,#1442);
#1199=LINE('',#8048,#1443);
#1200=LINE('',#8050,#1444);
#1201=LINE('',#8051,#1445);
#1202=LINE('',#8054,#1446);
#1203=LINE('',#8056,#1447);
#1204=LINE('',#8057,#1448);
#1205=LINE('',#8059,#1449);
#1206=LINE('',#8060,#1450);
#1427=VECTOR('',#5229,0.325);
#1428=VECTOR('',#5234,0.35);
#1429=VECTOR('',#5239,0.335);
#1430=VECTOR('',#5248,0.21);
#1431=VECTOR('',#5253,0.2);
#1432=VECTOR('',#5258,0.18);
#1433=VECTOR('',#5263,1.);
#1434=VECTOR('',#5264,1.);
#1435=VECTOR('',#5265,1.);
#1436=VECTOR('',#5266,1.);
#1437=VECTOR('',#5269,1.);
#1438=VECTOR('',#5270,1.);
#1439=VECTOR('',#5271,1.);
#1440=VECTOR('',#5274,1.);
#1441=VECTOR('',#5275,1.);
#1442=VECTOR('',#5276,1.);
#1443=VECTOR('',#5279,1.);
#1444=VECTOR('',#5280,1.);
#1445=VECTOR('',#5281,1.);
#1446=VECTOR('',#5284,1.);
#1447=VECTOR('',#5285,1.);
#1448=VECTOR('',#5286,1.);
#1449=VECTOR('',#5289,1.);
#1450=VECTOR('',#5290,1.);
#1677=CIRCLE('',#4289,0.3);
#1678=CIRCLE('',#4291,0.35);
#1679=CIRCLE('',#4293,0.35);
#1680=CIRCLE('',#4295,0.32);
#1681=CIRCLE('',#4297,0.22);
#1682=CIRCLE('',#4299,0.1954);
#1683=CIRCLE('',#4301,0.1954);
#1684=CIRCLE('',#4303,0.16);
#1909=VERTEX_POINT('',#7995);
#1910=VERTEX_POINT('',#7998);
#1911=VERTEX_POINT('',#8002);
#1912=VERTEX_POINT('',#8006);
#1913=VERTEX_POINT('',#8010);
#1914=VERTEX_POINT('',#8013);
#1915=VERTEX_POINT('',#8017);
#1916=VERTEX_POINT('',#8021);
#1917=VERTEX_POINT('',#8026);
#1918=VERTEX_POINT('',#8027);
#1919=VERTEX_POINT('',#8029);
#1920=VERTEX_POINT('',#8031);
#1921=VERTEX_POINT('',#8035);
#1922=VERTEX_POINT('',#8037);
#1923=VERTEX_POINT('',#8041);
#1924=VERTEX_POINT('',#8043);
#1925=VERTEX_POINT('',#8047);
#1926=VERTEX_POINT('',#8049);
#1927=VERTEX_POINT('',#8053);
#1928=VERTEX_POINT('',#8055);
#2307=EDGE_CURVE('',#1909,#1909,#1677,.T.);
#2308=EDGE_CURVE('',#1910,#1910,#1678,.T.);
#2309=EDGE_CURVE('',#1910,#1909,#1183,.T.);
#2310=EDGE_CURVE('',#1911,#1911,#1679,.T.);
#2311=EDGE_CURVE('',#1911,#1910,#1184,.T.);
#2312=EDGE_CURVE('',#1912,#1912,#1680,.T.);
#2313=EDGE_CURVE('',#1912,#1911,#1185,.T.);
#2314=EDGE_CURVE('',#1913,#1913,#1681,.T.);
#2315=EDGE_CURVE('',#1914,#1914,#1682,.F.);
#2316=EDGE_CURVE('',#1914,#1913,#1186,.T.);
#2317=EDGE_CURVE('',#1915,#1915,#1683,.F.);
#2318=EDGE_CURVE('',#1915,#1914,#1187,.T.);
#2319=EDGE_CURVE('',#1916,#1916,#1684,.T.);
#2320=EDGE_CURVE('',#1916,#1915,#1188,.T.);
#2321=EDGE_CURVE('',#1917,#1918,#1189,.T.);
#2322=EDGE_CURVE('',#1918,#1919,#1190,.T.);
#2323=EDGE_CURVE('',#1919,#1920,#1191,.T.);
#2324=EDGE_CURVE('',#1917,#1920,#1192,.T.);
#2325=EDGE_CURVE('',#1918,#1921,#1193,.T.);
#2326=EDGE_CURVE('',#1921,#1922,#1194,.T.);
#2327=EDGE_CURVE('',#1922,#1919,#1195,.T.);
#2328=EDGE_CURVE('',#1921,#1923,#1196,.T.);
#2329=EDGE_CURVE('',#1923,#1924,#1197,.T.);
#2330=EDGE_CURVE('',#1924,#1922,#1198,.T.);
#2331=EDGE_CURVE('',#1923,#1925,#1199,.T.);
#2332=EDGE_CURVE('',#1925,#1926,#1200,.T.);
#2333=EDGE_CURVE('',#1926,#1924,#1201,.T.);
#2334=EDGE_CURVE('',#1925,#1927,#1202,.T.);
#2335=EDGE_CURVE('',#1927,#1928,#1203,.T.);
#2336=EDGE_CURVE('',#1928,#1926,#1204,.T.);
#2337=EDGE_CURVE('',#1927,#1917,#1205,.T.);
#2338=EDGE_CURVE('',#1920,#1928,#1206,.T.);
#3062=ORIENTED_EDGE('',*,*,#2307,.F.);
#3063=ORIENTED_EDGE('',*,*,#2308,.F.);
#3064=ORIENTED_EDGE('',*,*,#2309,.T.);
#3065=ORIENTED_EDGE('',*,*,#2307,.T.);
#3066=ORIENTED_EDGE('',*,*,#2309,.F.);
#3067=ORIENTED_EDGE('',*,*,#2310,.F.);
#3068=ORIENTED_EDGE('',*,*,#2311,.T.);
#3069=ORIENTED_EDGE('',*,*,#2308,.T.);
#3070=ORIENTED_EDGE('',*,*,#2311,.F.);
#3071=ORIENTED_EDGE('',*,*,#2312,.F.);
#3072=ORIENTED_EDGE('',*,*,#2313,.T.);
#3073=ORIENTED_EDGE('',*,*,#2310,.T.);
#3074=ORIENTED_EDGE('',*,*,#2313,.F.);
#3075=ORIENTED_EDGE('',*,*,#2312,.T.);
#3076=ORIENTED_EDGE('',*,*,#2314,.F.);
#3077=ORIENTED_EDGE('',*,*,#2315,.F.);
#3078=ORIENTED_EDGE('',*,*,#2316,.T.);
#3079=ORIENTED_EDGE('',*,*,#2314,.T.);
#3080=ORIENTED_EDGE('',*,*,#2316,.F.);
#3081=ORIENTED_EDGE('',*,*,#2317,.F.);
#3082=ORIENTED_EDGE('',*,*,#2318,.T.);
#3083=ORIENTED_EDGE('',*,*,#2315,.T.);
#3084=ORIENTED_EDGE('',*,*,#2318,.F.);
#3085=ORIENTED_EDGE('',*,*,#2319,.F.);
#3086=ORIENTED_EDGE('',*,*,#2320,.T.);
#3087=ORIENTED_EDGE('',*,*,#2317,.T.);
#3088=ORIENTED_EDGE('',*,*,#2320,.F.);
#3089=ORIENTED_EDGE('',*,*,#2319,.T.);
#3090=ORIENTED_EDGE('',*,*,#2321,.T.);
#3091=ORIENTED_EDGE('',*,*,#2322,.T.);
#3092=ORIENTED_EDGE('',*,*,#2323,.T.);
#3093=ORIENTED_EDGE('',*,*,#2324,.F.);
#3094=ORIENTED_EDGE('',*,*,#2325,.T.);
#3095=ORIENTED_EDGE('',*,*,#2326,.T.);
#3096=ORIENTED_EDGE('',*,*,#2327,.T.);
#3097=ORIENTED_EDGE('',*,*,#2322,.F.);
#3098=ORIENTED_EDGE('',*,*,#2328,.T.);
#3099=ORIENTED_EDGE('',*,*,#2329,.T.);
#3100=ORIENTED_EDGE('',*,*,#2330,.T.);
#3101=ORIENTED_EDGE('',*,*,#2326,.F.);
#3102=ORIENTED_EDGE('',*,*,#2331,.T.);
#3103=ORIENTED_EDGE('',*,*,#2332,.T.);
#3104=ORIENTED_EDGE('',*,*,#2333,.T.);
#3105=ORIENTED_EDGE('',*,*,#2329,.F.);
#3106=ORIENTED_EDGE('',*,*,#2334,.T.);
#3107=ORIENTED_EDGE('',*,*,#2335,.T.);
#3108=ORIENTED_EDGE('',*,*,#2336,.T.);
#3109=ORIENTED_EDGE('',*,*,#2332,.F.);
#3110=ORIENTED_EDGE('',*,*,#2337,.T.);
#3111=ORIENTED_EDGE('',*,*,#2324,.T.);
#3112=ORIENTED_EDGE('',*,*,#2338,.T.);
#3113=ORIENTED_EDGE('',*,*,#2335,.F.);
#3114=ORIENTED_EDGE('',*,*,#2337,.F.);
#3115=ORIENTED_EDGE('',*,*,#2334,.F.);
#3116=ORIENTED_EDGE('',*,*,#2331,.F.);
#3117=ORIENTED_EDGE('',*,*,#2328,.F.);
#3118=ORIENTED_EDGE('',*,*,#2325,.F.);
#3119=ORIENTED_EDGE('',*,*,#2321,.F.);
#3120=ORIENTED_EDGE('',*,*,#2338,.F.);
#3121=ORIENTED_EDGE('',*,*,#2323,.F.);
#3122=ORIENTED_EDGE('',*,*,#2327,.F.);
#3123=ORIENTED_EDGE('',*,*,#2330,.F.);
#3124=ORIENTED_EDGE('',*,*,#2333,.F.);
#3125=ORIENTED_EDGE('',*,*,#2336,.F.);
#3431=CYLINDRICAL_SURFACE('',#4292,0.35);
#3432=CYLINDRICAL_SURFACE('',#4300,0.1954);
#3599=ADVANCED_FACE('',(#652),#444,.T.);
#3600=ADVANCED_FACE('',(#653),#149,.T.);
#3601=ADVANCED_FACE('',(#654),#3431,.T.);
#3602=ADVANCED_FACE('',(#655),#150,.T.);
#3603=ADVANCED_FACE('',(#656,#345),#445,.T.);
#3604=ADVANCED_FACE('',(#657),#151,.T.);
#3605=ADVANCED_FACE('',(#658),#3432,.T.);
#3606=ADVANCED_FACE('',(#659),#152,.T.);
#3607=ADVANCED_FACE('',(#660),#446,.T.);
#3608=ADVANCED_FACE('',(#661),#447,.F.);
#3609=ADVANCED_FACE('',(#662),#448,.F.);
#3610=ADVANCED_FACE('',(#663),#449,.F.);
#3611=ADVANCED_FACE('',(#664),#450,.F.);
#3612=ADVANCED_FACE('',(#665),#451,.F.);
#3613=ADVANCED_FACE('',(#666),#452,.F.);
#3614=ADVANCED_FACE('',(#667),#453,.F.);
#3615=ADVANCED_FACE('',(#668),#454,.F.);
#3693=CLOSED_SHELL('',(#3599,#3600,#3601,#3602,#3603,#3604,#3605,#3606,
#3607));
#3694=CLOSED_SHELL('',(#3608,#3609,#3610,#3611,#3612,#3613,#3614,#3615));
#4287=AXIS2_PLACEMENT_3D('',#7993,#5219,#5220);
#4288=AXIS2_PLACEMENT_3D('',#7994,#5221,#5222);
#4289=AXIS2_PLACEMENT_3D('',#7996,#5223,#5224);
#4290=AXIS2_PLACEMENT_3D('',#7997,#5225,#5226);
#4291=AXIS2_PLACEMENT_3D('',#7999,#5227,#5228);
#4292=AXIS2_PLACEMENT_3D('',#8001,#5230,#5231);
#4293=AXIS2_PLACEMENT_3D('',#8003,#5232,#5233);
#4294=AXIS2_PLACEMENT_3D('',#8005,#5235,#5236);
#4295=AXIS2_PLACEMENT_3D('',#8007,#5237,#5238);
#4296=AXIS2_PLACEMENT_3D('',#8009,#5240,#5241);
#4297=AXIS2_PLACEMENT_3D('',#8011,#5242,#5243);
#4298=AXIS2_PLACEMENT_3D('',#8012,#5244,#5245);
#4299=AXIS2_PLACEMENT_3D('',#8014,#5246,#5247);
#4300=AXIS2_PLACEMENT_3D('',#8016,#5249,#5250);
#4301=AXIS2_PLACEMENT_3D('',#8018,#5251,#5252);
#4302=AXIS2_PLACEMENT_3D('',#8020,#5254,#5255);
#4303=AXIS2_PLACEMENT_3D('',#8022,#5256,#5257);
#4304=AXIS2_PLACEMENT_3D('',#8024,#5259,#5260);
#4305=AXIS2_PLACEMENT_3D('',#8025,#5261,#5262);
#4306=AXIS2_PLACEMENT_3D('',#8034,#5267,#5268);
#4307=AXIS2_PLACEMENT_3D('',#8040,#5272,#5273);
#4308=AXIS2_PLACEMENT_3D('',#8046,#5277,#5278);
#4309=AXIS2_PLACEMENT_3D('',#8052,#5282,#5283);
#4310=AXIS2_PLACEMENT_3D('',#8058,#5287,#5288);
#4311=AXIS2_PLACEMENT_3D('',#8061,#5291,#5292);
#4312=AXIS2_PLACEMENT_3D('',#8062,#5293,#5294);
#5219=DIRECTION('axis',(0.,0.,1.));
#5220=DIRECTION('refdir',(1.,0.,0.));
#5221=DIRECTION('center_axis',(0.,1.,0.));
#5222=DIRECTION('ref_axis',(0.,0.,1.));
#5223=DIRECTION('center_axis',(0.,-1.,0.));
#5224=DIRECTION('ref_axis',(1.,0.,0.));
#5225=DIRECTION('center_axis',(0.,-1.,0.));
#5226=DIRECTION('ref_axis',(1.,0.,0.));
#5227=DIRECTION('center_axis',(0.,-1.,0.));
#5228=DIRECTION('ref_axis',(1.,0.,0.));
#5229=DIRECTION('',(0.707106781186547,0.707106781186548,8.65956056235493E-17));
#5230=DIRECTION('center_axis',(0.,-1.,0.));
#5231=DIRECTION('ref_axis',(1.,0.,0.));
#5232=DIRECTION('center_axis',(0.,-1.,0.));
#5233=DIRECTION('ref_axis',(1.,0.,0.));
#5234=DIRECTION('',(0.,1.,0.));
#5235=DIRECTION('center_axis',(0.,1.,0.));
#5236=DIRECTION('ref_axis',(1.,0.,0.));
#5237=DIRECTION('center_axis',(0.,-1.,0.));
#5238=DIRECTION('ref_axis',(1.,0.,0.));
#5239=DIRECTION('',(-0.707106781186547,0.707106781186548,-8.65956056235493E-17));
#5240=DIRECTION('center_axis',(0.,-1.,0.));
#5241=DIRECTION('ref_axis',(0.,0.,-1.));
#5242=DIRECTION('center_axis',(0.,-1.,0.));
#5243=DIRECTION('ref_axis',(1.,0.,0.));
#5244=DIRECTION('center_axis',(0.,1.,0.));
#5245=DIRECTION('ref_axis',(1.,0.,0.));
#5246=DIRECTION('center_axis',(0.,1.,0.));
#5247=DIRECTION('ref_axis',(1.,0.,0.));
#5248=DIRECTION('',(-0.447213595499958,0.894427190999916,-5.47678698264203E-17));
#5249=DIRECTION('center_axis',(0.,-1.,0.));
#5250=DIRECTION('ref_axis',(1.,0.,0.));
#5251=DIRECTION('center_axis',(0.,1.,0.));
#5252=DIRECTION('ref_axis',(1.,0.,0.));
#5253=DIRECTION('',(0.,1.,0.));
#5254=DIRECTION('center_axis',(0.,1.,0.));
#5255=DIRECTION('ref_axis',(1.,0.,0.));
#5256=DIRECTION('center_axis',(0.,-1.,0.));
#5257=DIRECTION('ref_axis',(1.,0.,0.));
#5258=DIRECTION('',(-0.707106781186547,0.707106781186548,-8.65956056235493E-17));
#5259=DIRECTION('center_axis',(0.,-1.,0.));
#5260=DIRECTION('ref_axis',(0.,0.,-1.));
#5261=DIRECTION('center_axis',(0.866025403784439,0.,-0.5));
#5262=DIRECTION('ref_axis',(0.5,0.,0.866025403784439));
#5263=DIRECTION('',(-0.5,0.,-0.866025403784439));
#5264=DIRECTION('',(0.,-1.,0.));
#5265=DIRECTION('',(0.5,0.,0.866025403784439));
#5266=DIRECTION('',(0.,-1.,0.));
#5267=DIRECTION('center_axis',(1.60246890531964E-16,0.,-1.));
#5268=DIRECTION('ref_axis',(1.,0.,1.60246890531964E-16));
#5269=DIRECTION('',(-1.,0.,-1.60246890531964E-16));
#5270=DIRECTION('',(0.,-1.,0.));
#5271=DIRECTION('',(1.,0.,1.60246890531964E-16));
#5272=DIRECTION('center_axis',(-0.866025403784439,0.,-0.5));
#5273=DIRECTION('ref_axis',(0.5,0.,-0.866025403784439));
#5274=DIRECTION('',(-0.5,0.,0.866025403784439));
#5275=DIRECTION('',(0.,-1.,0.));
#5276=DIRECTION('',(0.5,0.,-0.866025403784439));
#5277=DIRECTION('center_axis',(-0.866025403784439,0.,0.5));
#5278=DIRECTION('ref_axis',(-0.5,0.,-0.866025403784439));
#5279=DIRECTION('',(0.5,0.,0.866025403784439));
#5280=DIRECTION('',(0.,-1.,0.));
#5281=DIRECTION('',(-0.5,0.,-0.866025403784439));
#5282=DIRECTION('center_axis',(-1.60246890531964E-16,0.,1.));
#5283=DIRECTION('ref_axis',(-1.,0.,-1.60246890531964E-16));
#5284=DIRECTION('',(1.,0.,1.60246890531964E-16));
#5285=DIRECTION('',(0.,-1.,0.));
#5286=DIRECTION('',(-1.,0.,-1.60246890531964E-16));
#5287=DIRECTION('center_axis',(0.866025403784439,0.,0.5));
#5288=DIRECTION('ref_axis',(-0.5,0.,0.866025403784439));
#5289=DIRECTION('',(0.5,0.,-0.866025403784439));
#5290=DIRECTION('',(-0.5,0.,0.866025403784439));
#5291=DIRECTION('center_axis',(0.,1.,0.));
#5292=DIRECTION('ref_axis',(1.,0.,0.));
#5293=DIRECTION('center_axis',(0.,-1.,0.));
#5294=DIRECTION('ref_axis',(0.,0.,-1.));
#7993=CARTESIAN_POINT('',(0.,0.,0.));
#7994=CARTESIAN_POINT('Origin',(0.3,0.4,0.));
#7995=CARTESIAN_POINT('',(-0.3,0.4,-3.67394039744206E-17));
#7996=CARTESIAN_POINT('Origin',(0.,0.4,0.));
#7997=CARTESIAN_POINT('Origin',(0.,0.375,0.));
#7998=CARTESIAN_POINT('',(-0.35,0.35,-4.28626379701573E-17));
#7999=CARTESIAN_POINT('Origin',(0.,0.35,0.));
#8000=CARTESIAN_POINT('',(-0.325,0.375,-3.9801020972289E-17));
#8001=CARTESIAN_POINT('Origin',(0.,0.19,0.));
#8002=CARTESIAN_POINT('',(-0.35,0.03,-4.28626379701574E-17));
#8003=CARTESIAN_POINT('Origin',(0.,0.03,0.));
#8004=CARTESIAN_POINT('',(-0.35,0.19,-4.28626379701574E-17));
#8005=CARTESIAN_POINT('Origin',(0.,0.0149999999999999,0.));
#8006=CARTESIAN_POINT('',(-0.32,-3.29597460435593E-17,-3.91886975727153E-17));
#8007=CARTESIAN_POINT('Origin',(0.,0.,0.));
#8008=CARTESIAN_POINT('',(-0.335,0.0149999999999999,-4.10256677714363E-17));
#8009=CARTESIAN_POINT('Origin',(0.22,0.,0.));
#8010=CARTESIAN_POINT('',(-0.22,-6.93889390390723E-18,-2.69422295812418E-17));
#8011=CARTESIAN_POINT('Origin',(0.,0.,0.));
#8012=CARTESIAN_POINT('Origin',(0.,-0.02,0.));
#8013=CARTESIAN_POINT('',(-0.1954,-0.0492,2.39295984553393E-17));
#8014=CARTESIAN_POINT('Origin',(0.,-0.0492,0.));
#8015=CARTESIAN_POINT('',(-0.21,-0.02,-2.57175827820944E-17));
#8016=CARTESIAN_POINT('Origin',(0.,-0.8,0.));
#8017=CARTESIAN_POINT('',(-0.1954,-1.5646,2.39295984553393E-17));
#8018=CARTESIAN_POINT('Origin',(0.,-1.5646,0.));
#8019=CARTESIAN_POINT('',(-0.1954,-0.8,-2.39295984553393E-17));
#8020=CARTESIAN_POINT('Origin',(0.,-1.58,0.));
#8021=CARTESIAN_POINT('',(-0.16,-1.6,-1.95943487863577E-17));
#8022=CARTESIAN_POINT('Origin',(0.,-1.6,0.));
#8023=CARTESIAN_POINT('',(-0.18,-1.58,-2.20436423846524E-17));
#8024=CARTESIAN_POINT('Origin',(0.,-1.6,0.));
#8025=CARTESIAN_POINT('Origin',(0.0866025403784439,-0.4,-0.15));
#8026=CARTESIAN_POINT('',(0.173205080756888,-0.4,0.));
#8027=CARTESIAN_POINT('',(0.0866025403784439,-0.4,-0.15));
#8028=CARTESIAN_POINT('',(0.173205080756888,-0.4,0.));
#8029=CARTESIAN_POINT('',(0.0866025403784439,-0.64,-0.15));
#8030=CARTESIAN_POINT('',(0.0866025403784439,-0.4,-0.15));
#8031=CARTESIAN_POINT('',(0.173205080756888,-0.64,0.));
#8032=CARTESIAN_POINT('',(0.173205080756888,-0.64,0.));
#8033=CARTESIAN_POINT('',(0.173205080756888,-0.4,0.));
#8034=CARTESIAN_POINT('Origin',(-0.0866025403784438,-0.4,-0.15));
#8035=CARTESIAN_POINT('',(-0.0866025403784438,-0.4,-0.15));
#8036=CARTESIAN_POINT('',(0.0866025403784439,-0.4,-0.15));
#8037=CARTESIAN_POINT('',(-0.0866025403784438,-0.64,-0.15));
#8038=CARTESIAN_POINT('',(-0.0866025403784438,-0.4,-0.15));
#8039=CARTESIAN_POINT('',(0.0866025403784439,-0.64,-0.15));
#8040=CARTESIAN_POINT('Origin',(-0.173205080756888,-0.4,-2.77555756156289E-17));
#8041=CARTESIAN_POINT('',(-0.173205080756888,-0.4,-2.12115047744981E-17));
#8042=CARTESIAN_POINT('',(-0.0866025403784438,-0.4,-0.15));
#8043=CARTESIAN_POINT('',(-0.173205080756888,-0.64,-2.77555756156289E-17));
#8044=CARTESIAN_POINT('',(-0.173205080756888,-0.4,-2.12115047744981E-17));
#8045=CARTESIAN_POINT('',(-0.0866025403784438,-0.64,-0.15));
#8046=CARTESIAN_POINT('Origin',(-0.0866025403784439,-0.4,0.15));
#8047=CARTESIAN_POINT('',(-0.0866025403784439,-0.4,0.15));
#8048=CARTESIAN_POINT('',(-0.173205080756888,-0.4,-2.12115047744981E-17));
#8049=CARTESIAN_POINT('',(-0.0866025403784439,-0.64,0.15));
#8050=CARTESIAN_POINT('',(-0.0866025403784439,-0.4,0.15));
#8051=CARTESIAN_POINT('',(-0.173205080756888,-0.64,-2.12115047744981E-17));
#8052=CARTESIAN_POINT('Origin',(0.0866025403784439,-0.4,0.15));
#8053=CARTESIAN_POINT('',(0.0866025403784439,-0.4,0.15));
#8054=CARTESIAN_POINT('',(-0.0866025403784439,-0.4,0.15));
#8055=CARTESIAN_POINT('',(0.0866025403784439,-0.64,0.15));
#8056=CARTESIAN_POINT('',(0.0866025403784439,-0.4,0.15));
#8057=CARTESIAN_POINT('',(-0.0866025403784439,-0.64,0.15));
#8058=CARTESIAN_POINT('Origin',(0.173205080756888,-0.4,0.));
#8059=CARTESIAN_POINT('',(0.0866025403784439,-0.4,0.15));
#8060=CARTESIAN_POINT('',(0.0866025403784439,-0.64,0.15));
#8061=CARTESIAN_POINT('Origin',(0.,-0.4,-2.77555756156289E-17));
#8062=CARTESIAN_POINT('Origin',(0.,-0.64,-2.77555756156289E-17));
#8396=UNCERTAINTY_MEASURE_WITH_UNIT(LENGTH_MEASURE(0.001),#8429,
'DISTANCE_ACCURACY_VALUE',
'Maximum model space distance between geometric entities at asserted c
onnectivities');
#8402=UNCERTAINTY_MEASURE_WITH_UNIT(LENGTH_MEASURE(0.001),#8429,
'DISTANCE_ACCURACY_VALUE',
'Maximum model space distance between geometric entities at asserted c
onnectivities');
#8422=(
GEOMETRIC_REPRESENTATION_CONTEXT(3)
GLOBAL_UNCERTAINTY_ASSIGNED_CONTEXT((#8396))
GLOBAL_UNIT_ASSIGNED_CONTEXT((#8429,#8431,#8432))
REPRESENTATION_CONTEXT('','3D')
);
#8428=(
GEOMETRIC_REPRESENTATION_CONTEXT(3)
GLOBAL_UNCERTAINTY_ASSIGNED_CONTEXT((#8402))
GLOBAL_UNIT_ASSIGNED_CONTEXT((#8429,#8431,#8432))
REPRESENTATION_CONTEXT('','3D')
);
#8429=(
LENGTH_UNIT()
NAMED_UNIT(*)
SI_UNIT(.CENTI.,.METRE.)
);
#8431=(
NAMED_UNIT(*)
PLANE_ANGLE_UNIT()
SI_UNIT($,.RADIAN.)
);
#8432=(
NAMED_UNIT(*)
SI_UNIT($,.STERADIAN.)
SOLID_ANGLE_UNIT()
);
#8452=SHAPE_DEFINITION_REPRESENTATION(#8477,#8533);
#8477=PRODUCT_DEFINITION_SHAPE('',$,#8559);
#8533=SHAPE_REPRESENTATION('',(#4287),#8422);
#8539=PRODUCT_DEFINITION_CONTEXT('part definition',#8616,'design');
#8559=PRODUCT_DEFINITION('Cap Screw - M4x16','Cap Screw - M4x16',
#8584,#8539);
#8584=PRODUCT_DEFINITION_FORMATION('',$,#8637);
#8616=APPLICATION_CONTEXT(
'Core Data for Automotive Mechanical Design Process');
#8617=PRODUCT_CONTEXT('part definition',#8616,'mechanical');
#8637=PRODUCT('Cap Screw - M4x16','Cap Screw - M4x16',
'Cap Screw - M4x16',(#8617));
#8706=COLOUR_RGB('Black',0.12,0.14,0.17);
#8707=FILL_AREA_STYLE_COLOUR('',#8706);
#8708=FILL_AREA_STYLE('',(#8707));
#8709=SURFACE_STYLE_FILL_AREA(#8708);
#8710=SURFACE_SIDE_STYLE('',(#8709));
#8711=SURFACE_STYLE_USAGE(.BOTH.,#8710);
#8712=PRESENTATION_STYLE_ASSIGNMENT((#8711));
ENDSEC;
END-ISO-10303-21;
